ISO-10303-21;
HEADER;
FILE_DESCRIPTION (('STEP AP214'),
    '1' );
FILE_NAME ('Lock nut.step',
    '2026-10-06T08:09:25',
    ( '' ),
    ( '' ),
    'SwSTEP 2.0',
    'SolidWorks 2021',
    '' );
FILE_SCHEMA (( 'AUTOMOTIVE_DESIGN' ));
ENDSEC;

DATA;
#53=CARTESIAN_POINT ( 'NONE',  ( 5.773502691896164052, 4.999999999999978684, 4.999999999999978684 ) ) ;
#117=CONICAL_SURFACE ( 'NONE', #18527, 7.499999999999998224, 1.308996938995750092 ) ;
#203=ORIENTED_EDGE ( 'NONE', *, *, #5369, .T. ) ;
#252=CARTESIAN_POINT ( 'NONE',  ( -4.330127018922255822, -9.714451465470119729E-14, 7.499999999999985789 ) ) ;
#339=EDGE_LOOP ( 'NONE', ( #16381, #10747, #21363, #15914, #5920, #9620 ) ) ;
#372=MECHANICAL_DESIGN_GEOMETRIC_PRESENTATION_REPRESENTATION('',(#4867),#22164);
#438=CARTESIAN_POINT ( 'NONE',  ( -2.886699270652919314, 4.864326267994432129, -7.500000000000002665 ) ) ;
#462=CARTESIAN_POINT ( 'NONE',  ( 7.216878364870271234, 4.999999999999979572, -2.499999999999973799 ) ) ;
#475=B_SPLINE_CURVE_WITH_KNOTS ( 'NONE', 3,
 ( #19236, #2894, #11596, #1255 ),
 .UNSPECIFIED., .F., .F.,
 ( 4, 4 ),
 ( 0.01659225151561716932, 0.02095135962594951370 ),
 .UNSPECIFIED. ) ;
#507=CARTESIAN_POINT ( 'NONE',  ( 0.000000000000000000, 0.000000000000000000, 0.000000000000000000 ) ) ;
#574=CARTESIAN_POINT ( 'NONE',  ( 0.000000000000000000, 0.000000000000000000, 0.000000000000000000 ) ) ;
#596=ORIENTED_EDGE ( 'NONE', *, *, #22450, .T. ) ;
#632=ORIENTED_EDGE ( 'NONE', *, *, #18856, .T. ) ;
#672=DIRECTION ( 'NONE',  ( -9.693457064947022734E-26, 0.000000000000000000, 1.000000000000000000 ) ) ;
#724=PRESENTATION_STYLE_ASSIGNMENT (( #18824 ) ) ;
#733=CARTESIAN_POINT ( 'NONE',  ( -6.938893903907228378E-14, 4.999999999999976907, -4.163336342344337027E-14 ) ) ;
#741=( NAMED_UNIT ( * ) SI_UNIT ( $, .STERADIAN. ) SOLID_ANGLE_UNIT ( ) );
#822=CARTESIAN_POINT ( 'NONE',  ( -4.330127018922234505, 4.689110867544671102, -7.500000000000000000 ) ) ;
#844=CARTESIAN_POINT ( 'NONE',  ( -8.326672684688674053E-14, 4.999999999999893419, 7.499999999999958256 ) ) ;
#849=AXIS2_PLACEMENT_3D ( 'NONE', #4850, #17199, #11796 ) ;
#953=CIRCLE ( 'NONE', #7713, 7.499999999999998224 ) ;
#954=EDGE_LOOP ( 'NONE', ( #18047, #18944, #13136, #596, #6750, #15540 ) ) ;
#957=FACE_OUTER_BOUND ( 'NONE', #16219, .T. ) ;
#1002=ORIENTED_EDGE ( 'NONE', *, *, #23103, .F. ) ;
#1026=VECTOR ( 'NONE', #15890, 1000.000000000000000 ) ;
#1035=VERTEX_POINT ( 'NONE', #6220 ) ;
#1055=DIRECTION ( 'NONE',  ( 9.693522803355793065E-26, -5.963788443470848352E-28, -1.000000000000000000 ) ) ;
#1109=DIRECTION ( 'NONE',  ( -0.4999999999999999445, -2.286725509617068974E-17, 0.8660254037844387076 ) ) ;
#1202=SURFACE_STYLE_USAGE ( .BOTH. , #9911 ) ;
#1218=CARTESIAN_POINT ( 'NONE',  ( 4.330127018922088844, -1.387778780781445676E-13, 7.500000000000027534 ) ) ;
#1255=CARTESIAN_POINT ( 'NONE',  ( -4.857225732735059864E-14, 4.999999999999976907, -7.500000000000003553 ) ) ;
#1290=CARTESIAN_POINT ( 'NONE',  ( -6.938893903907228378E-14, 4.999999999999976907, -4.163336342344337027E-14 ) ) ;
#1315=PLANE ( 'NONE',  #14813 ) ;
#1358=EDGE_CURVE ( 'NONE', #10173, #15286, #5089, .T. ) ;
#1399=EDGE_CURVE ( 'NONE', #12860, #8601, #3217, .T. ) ;
#1487=EDGE_CURVE ( 'NONE', #12036, #18303, #13685, .T. ) ;
#1496=EDGE_CURVE ( 'NONE', #4163, #4944, #19088, .T. ) ;
#1554=DIRECTION ( 'NONE',  ( -5.551115123561405253E-17, -1.000000000000000000, -2.256980353643891447E-27 ) ) ;
#1625=LINE ( 'NONE', #7049, #5406 ) ;
#1629=CARTESIAN_POINT ( 'NONE',  ( -8.660254037844428154, 4.689110867544629357, -1.387778780781445676E-14 ) ) ;
#1732=FACE_OUTER_BOUND ( 'NONE', #21728, .T. ) ;
#1940=B_SPLINE_CURVE_WITH_KNOTS ( 'NONE', 3,
 ( #6145, #13319, #14419, #20501 ),
 .UNSPECIFIED., .F., .F.,
 ( 4, 4 ),
 ( 0.01162760039383341909, 0.01599369037747973635 ),
 .UNSPECIFIED. ) ;
#2039=EDGE_LOOP ( 'NONE', ( #11308, #14115, #3123 ) ) ;
#2069=CARTESIAN_POINT ( 'NONE',  ( -8.660254037844421049, 4.999999999999948486, -1.387778780781445676E-14 ) ) ;
#2071=DIRECTION ( 'NONE',  ( 9.693522803355793065E-26, -5.963788443470848352E-28, -1.000000000000000000 ) ) ;
#2194=DIRECTION ( 'NONE',  ( -9.693457064947022734E-26, 0.000000000000000000, 1.000000000000000000 ) ) ;
#2200=CARTESIAN_POINT ( 'NONE',  ( -1.442209863900529188, 4.971646688682866078, -7.500000000000002665 ) ) ;
#2287=AXIS2_PLACEMENT_3D ( 'NONE', #10010, #15175, #20361 ) ;
#2291=ORIENTED_EDGE ( 'NONE', *, *, #18696, .F. ) ;
#2304=CARTESIAN_POINT ( 'NONE',  ( 7.938566201357266650, 4.882486540518886642, 1.249999999999969580 ) ) ;
#2324=DIRECTION ( 'NONE',  ( 5.551115123561405253E-17, 1.000000000000000000, -5.963788443470795439E-28 ) ) ;
#2407=CIRCLE ( 'NONE', #8815, 7.500000000000001776 ) ;
#2414=ORIENTED_EDGE ( 'NONE', *, *, #22450, .F. ) ;
#2415=EDGE_LOOP ( 'NONE', ( #20282, #16350, #16925, #203, #3355, #16891 ) ) ;
#2425=CARTESIAN_POINT ( 'NONE',  ( -7.216878364870317419, 5.000000000000001776, -2.499999999999978240 ) ) ;
#2433=ADVANCED_BREP_SHAPE_REPRESENTATION ( '', ( #13118, #22115 ), #12003 ) ;
#2480=CARTESIAN_POINT ( 'NONE',  ( -1.442209863900557387, 4.971646688682839432, 7.500000000000007105 ) ) ;
#2498=EDGE_CURVE ( 'NONE', #9471, #23120, #9205, .T. ) ;
#2506=CARTESIAN_POINT ( 'NONE',  ( -6.495190528383341544, 4.999999999999920952, 3.750000000000017319 ) ) ;
#2600=DIRECTION ( 'NONE',  ( 5.551115123561405253E-17, 1.000000000000000000, 2.256980353643891447E-27 ) ) ;
#2606=CARTESIAN_POINT ( 'NONE',  ( 8.660254037844413944, 4.689110867544616035, 2.775557561562891351E-14 ) ) ;
#2612=ORIENTED_EDGE ( 'NONE', *, *, #20821, .T. ) ;
#2645=EDGE_LOOP ( 'NONE', ( #17463, #13928, #18590 ) ) ;
#2678=DIRECTION ( 'NONE',  ( -9.693522803355793065E-26, 5.963788443470849249E-28, 1.000000000000000000 ) ) ;
#2850=ORIENTED_EDGE ( 'NONE', *, *, #8237, .F. ) ;
#2894=CARTESIAN_POINT ( 'NONE',  ( 2.889332061078578651, 4.882140790251139784, -7.500000000000003553 ) ) ;
#2963=DIRECTION ( 'NONE',  ( 0.000000000000000000, 0.000000000000000000, 1.000000000000000000 ) ) ;
#2979=CARTESIAN_POINT ( 'NONE',  ( -4.330127018922199866, 4.999999999999920952, 7.500000000000007105 ) ) ;
#3118=CIRCLE ( 'NONE', #849, 4.750000000000000000 ) ;
#3123=ORIENTED_EDGE ( 'NONE', *, *, #14408, .F. ) ;
#3132=LINE ( 'NONE', #10415, #12828 ) ;
#3206=PRODUCT_CONTEXT ( 'NONE', #11146, 'mechanical' ) ;
#3217=LINE ( 'NONE', #1218, #1026 ) ;
#3239=ORIENTED_EDGE ( 'NONE', *, *, #8923, .F. ) ;
#3355=ORIENTED_EDGE ( 'NONE', *, *, #21250, .F. ) ;
#3356=ADVANCED_FACE ( 'NONE', ( #20467 ), #16910, .F. ) ;
#3368=CARTESIAN_POINT ( 'NONE',  ( -6.938893903861184144E-14, 0.7368602791855416445, -4.750000000000013323 ) ) ;
#3384=ORIENTED_EDGE ( 'NONE', *, *, #3742, .T. ) ;
#3400=CARTESIAN_POINT ( 'NONE',  ( 0.000000000000000000, 0.000000000000000000, 0.000000000000000000 ) ) ;
#3420=LINE ( 'NONE', #8830, #19196 ) ;
#3453=LINE ( 'NONE', #10390, #10772 ) ;
#3486=ORIENTED_EDGE ( 'NONE', *, *, #20226, .T. ) ;
#3537=CARTESIAN_POINT ( 'NONE',  ( 6.495190528383244732, 4.999999999999948486, -3.750000000000000000 ) ) ;
#3686=EDGE_LOOP ( 'NONE', ( #21000, #8639, #12506 ) ) ;
#3700=DIRECTION ( 'NONE',  ( -5.551115123561405253E-17, -1.000000000000000000, -2.256980353643891447E-27 ) ) ;
#3742=EDGE_CURVE ( 'NONE', #16003, #3791, #13390, .T. ) ;
#3791=VERTEX_POINT ( 'NONE', #6319 ) ;
#3807=CARTESIAN_POINT ( 'NONE',  ( -6.938893903907228378E-15, -2.775557561562891351E-14, -7.500000000000000000 ) ) ;
#3818=DIRECTION ( 'NONE',  ( 5.551115123561405253E-17, 1.000000000000000000, -5.963788443470795439E-28 ) ) ;
#3836=CARTESIAN_POINT ( 'NONE',  ( 6.495190528383244732, 4.999999999999948486, -3.750000000000000000 ) ) ;
#3870=CARTESIAN_POINT ( 'NONE',  ( -6.938893903907228378E-14, 4.999999999999976907, -4.163336342344337027E-14 ) ) ;
#3878=STYLED_ITEM ( 'NONE', ( #724 ), #13118 ) ;
#3881=EDGE_CURVE ( 'NONE', #7229, #16003, #475, .T. ) ;
#3927=DIRECTION ( 'NONE',  ( 5.551115123561405253E-17, 1.000000000000000000, -5.963788443470795439E-28 ) ) ;
#3959=CARTESIAN_POINT ( 'NONE',  ( -0.7206956945560391015, 4.999999999999988454, -7.500000000000003553 ) ) ;
#3966=DIRECTION ( 'NONE',  ( -5.551115123561405253E-17, -1.000000000000000000, -2.256980353643891447E-27 ) ) ;
#4055=PLANE ( 'NONE',  #11234 ) ;
#4068=DIRECTION ( 'NONE',  ( -0.4999999999999998335, -4.767331059895059913E-16, -0.8660254037844387076 ) ) ;
#4117=EDGE_LOOP ( 'NONE', ( #7484, #18129 ) ) ;
#4163=VERTEX_POINT ( 'NONE', #11229 ) ;
#4172=PLANE ( 'NONE',  #18509 ) ;
#4245=ORIENTED_EDGE ( 'NONE', *, *, #12674, .F. ) ;
#4355=PLANE ( 'NONE',  #17557 ) ;
#4373=CARTESIAN_POINT ( 'NONE',  ( 4.330127018922088844, -1.387778780781445676E-13, 7.500000000000027534 ) ) ;
#4399=ORIENTED_EDGE ( 'NONE', *, *, #19458, .F. ) ;
#4405=CARTESIAN_POINT ( 'NONE',  ( -8.660254037844406838, 0.000000000000000000, 6.938893903907228378E-15 ) ) ;
#4562=AXIS2_PLACEMENT_3D ( 'NONE', #11730, #21986, #2678 ) ;
#4563=CARTESIAN_POINT ( 'NONE',  ( -5.773502691896256422, 5.000000000000003553, -4.999999999999975131 ) ) ;
#4599=FILL_AREA_STYLE ('',( #11542 ) ) ;
#4647=DIRECTION ( 'NONE',  ( -5.551115123561405253E-17, -1.000000000000000000, -2.256980353643891447E-27 ) ) ;
#4657=CARTESIAN_POINT ( 'NONE',  ( -4.330127018922234505, -2.775557561562891351E-14, -7.499999999999989342 ) ) ;
#4723=VECTOR ( 'NONE', #1109, 1000.000000000000000 ) ;
#4772=FACE_OUTER_BOUND ( 'NONE', #18415, .T. ) ;
#4810=ADVANCED_FACE ( 'NONE', ( #1732 ), #8482, .T. ) ;
#4823=CARTESIAN_POINT ( 'NONE',  ( 0.000000000000000000, 0.000000000000000000, 0.000000000000000000 ) ) ;
#4850=CARTESIAN_POINT ( 'NONE',  ( -6.938893903907228378E-14, 0.7368602791855416445, -1.387778780781445676E-14 ) ) ;
#4867=STYLED_ITEM ( 'NONE', ( #9786 ), #2433 ) ;
#4901=EDGE_CURVE ( 'NONE', #10858, #11150, #7606, .T. ) ;
#4909=FACE_BOUND ( 'NONE', #4117, .T. ) ;
#4943=CARTESIAN_POINT ( 'NONE',  ( 0.000000000000000000, 0.000000000000000000, 0.000000000000000000 ) ) ;
#4944=VERTEX_POINT ( 'NONE', #8538 ) ;
#5004=CARTESIAN_POINT ( 'NONE',  ( -6.495190528383328221, -4.163336342344337027E-14, 3.750000000000038192 ) ) ;
#5011=ORIENTED_EDGE ( 'NONE', *, *, #16231, .T. ) ;
#5028=CARTESIAN_POINT ( 'NONE',  ( -6.892555770682806857E-14, 0.7368602791855416445, 4.749999999999985789 ) ) ;
#5035=DIRECTION ( 'NONE',  ( -0.4999999999999999445, -2.286725509617068974E-17, 0.8660254037844387076 ) ) ;
#5050=ORIENTED_EDGE ( 'NONE', *, *, #1487, .T. ) ;
#5089=LINE ( 'NONE', #17664, #17153 ) ;
#5136=ORIENTED_EDGE ( 'NONE', *, *, #8237, .T. ) ;
#5177=CARTESIAN_POINT ( 'NONE',  ( -5.773502691896283068, 4.999999999999979572, 4.999999999999997335 ) ) ;
#5306=DIRECTION ( 'NONE',  ( 1.000000000000000000, 0.000000000000000000, 0.000000000000000000 ) ) ;
#5332=AXIS2_PLACEMENT_3D ( 'NONE', #20900, #6892, #6430 ) ;
#5354=B_SPLINE_CURVE_WITH_KNOTS ( 'NONE', 3,
 ( #14950, #12964, #12842, #2480, #20367, #844 ),
 .UNSPECIFIED., .F., .F.,
 ( 4, 2, 4 ),
 ( 0.007276530541002032039, 0.009452065467417725131, 0.01162760039383341909 ),
 .UNSPECIFIED. ) ;
#5369=EDGE_CURVE ( 'NONE', #8601, #5408, #22867, .T. ) ;
#5406=VECTOR ( 'NONE', #5035, 1000.000000000000000 ) ;
#5408=VERTEX_POINT ( 'NONE', #13694 ) ;
#5504=CARTESIAN_POINT ( 'NONE',  ( 9.184850986335003870E-16, 4.472790346437877718E-27, 7.499999999999998224 ) ) ;
#5511=CARTESIAN_POINT ( 'NONE',  ( -7.938566201357386554, 4.882486540518891971, 1.249999999999988898 ) ) ;
#5520=CARTESIAN_POINT ( 'NONE',  ( -6.938893903907228378E-14, 4.999999999999976907, -4.163336342344337027E-14 ) ) ;
#5544=DIRECTION ( 'NONE',  ( 0.4999999999999999445, 4.767331059895059913E-16, 0.8660254037844387076 ) ) ;
#5549=ORIENTED_EDGE ( 'NONE', *, *, #18330, .F. ) ;
#5568=AXIS2_PLACEMENT_3D ( 'NONE', #17894, #21777, #5544 ) ;
#5579=UNCERTAINTY_MEASURE_WITH_UNIT (LENGTH_MEASURE( 1.000000000000000082E-05 ), #6129, 'distance_accuracy_value', 'NONE');
#5662=DIRECTION ( 'NONE',  ( 9.693522803355793065E-26, -5.963788443470848352E-28, -1.000000000000000000 ) ) ;
#5688=DIRECTION ( 'NONE',  ( 1.001543064812511222E-16, 2.634795423438190192E-27, -1.000000000000000000 ) ) ;
#5748=CARTESIAN_POINT ( 'NONE',  ( 4.330127018922110160, 4.999999999999976907, -7.500000000000003553 ) ) ;
#5819=CIRCLE ( 'NONE', #13681, 4.750000000000000000 ) ;
#5844=UNCERTAINTY_MEASURE_WITH_UNIT (LENGTH_MEASURE( 1.000000000000000082E-05 ), #18615, 'distance_accuracy_value', 'NONE');
#5885=FACE_OUTER_BOUND ( 'NONE', #14283, .T. ) ;
#5910=DIRECTION ( 'NONE',  ( 9.693522803355793065E-26, -5.963788443470848352E-28, -1.000000000000000000 ) ) ;
#5920=ORIENTED_EDGE ( 'NONE', *, *, #1496, .F. ) ;
#5963=ADVANCED_FACE ( 'NONE', ( #5885 ), #11581, .T. ) ;
#5984=DIRECTION ( 'NONE',  ( -9.693457064947022734E-26, 0.000000000000000000, 1.000000000000000000 ) ) ;
#6002=DIRECTION ( 'NONE',  ( 5.551115123561405253E-17, 1.000000000000000000, -5.963788443470795439E-28 ) ) ;
#6015=( NAMED_UNIT ( * ) PLANE_ANGLE_UNIT ( ) SI_UNIT ( $, .RADIAN. ) );
#6049=DIRECTION ( 'NONE',  ( 9.693522803355793065E-26, -5.963788443470848352E-28, -1.000000000000000000 ) ) ;
#6067=EDGE_CURVE ( 'NONE', #20666, #11557, #19820, .T. ) ;
#6100=CARTESIAN_POINT ( 'NONE',  ( 6.495190528383244732, 4.999999999999935163, 3.750000000000003553 ) ) ;
#6129=( LENGTH_UNIT ( ) NAMED_UNIT ( * ) SI_UNIT ( .MILLI., .METRE. ) );
#6145=CARTESIAN_POINT ( 'NONE',  ( -8.326672684688674053E-14, 4.999999999999893419, 7.499999999999958256 ) ) ;
#6165=AXIS2_PLACEMENT_3D ( 'NONE', #20712, #17160, #15282 ) ;
#6220=CARTESIAN_POINT ( 'NONE',  ( 4.330127018922110160, -5.551115123125782702E-14, -7.499999999999996447 ) ) ;
#6229=CARTESIAN_POINT ( 'NONE',  ( 0.000000000000000000, 0.000000000000000000, 0.000000000000000000 ) ) ;
#6235=CARTESIAN_POINT ( 'NONE',  ( 8.660254037844337560, 4.999999999999948486, 2.775557561562891351E-14 ) ) ;
#6242=EDGE_LOOP ( 'NONE', ( #14049, #5136, #11701, #22584 ) ) ;
#6267=ORIENTED_EDGE ( 'NONE', *, *, #9806, .F. ) ;
#6281=AXIS2_PLACEMENT_3D ( 'NONE', #20033, #5688, #12852 ) ;
#6319=CARTESIAN_POINT ( 'NONE',  ( -4.330127018922234505, 4.689110867544671102, -7.500000000000000000 ) ) ;
#6366=( NAMED_UNIT ( * ) SI_UNIT ( $, .STERADIAN. ) SOLID_ANGLE_UNIT ( ) );
#6372=CIRCLE ( 'NONE', #14624, 7.500000000000001776 ) ;
#6386=( NAMED_UNIT ( * ) SI_UNIT ( $, .STERADIAN. ) SOLID_ANGLE_UNIT ( ) );
#6430=DIRECTION ( 'NONE',  ( -9.693457064947022734E-26, 0.000000000000000000, 1.000000000000000000 ) ) ;
#6459=AXIS2_PLACEMENT_3D ( 'NONE', #574, #2324, #9502 ) ;
#6462=LINE ( 'NONE', #6235, #20897 ) ;
#6479=DIRECTION ( 'NONE',  ( -5.551115123561405253E-17, -1.000000000000000000, -2.256980353643891447E-27 ) ) ;
#6553=CARTESIAN_POINT ( 'NONE',  ( -6.892555770682806857E-14, 4.999999999999976907, 4.749999999999958256 ) ) ;
#6658=DIRECTION ( 'NONE',  ( 0.8660254037844387076, 2.858508811740733972E-17, 0.4999999999999998890 ) ) ;
#6671=PRODUCT_DEFINITION_SHAPE ( 'NONE', 'NONE',  #20858 ) ;
#6750=ORIENTED_EDGE ( 'NONE', *, *, #7539, .F. ) ;
#6759=DIRECTION ( 'NONE',  ( 5.551115123561405253E-17, 1.000000000000000000, 2.256980353643891447E-27 ) ) ;
#6765=ADVANCED_FACE ( 'NONE', ( #16821 ), #4355, .F. ) ;
#6892=DIRECTION ( 'NONE',  ( -5.551115123561405253E-17, -1.000000000000000000, -2.256980353643891447E-27 ) ) ;
#6904=MECHANICAL_DESIGN_GEOMETRIC_PRESENTATION_REPRESENTATION('',(#3878),#15150);
#6981=DIRECTION ( 'NONE',  ( -5.551115123561405253E-17, -1.000000000000000000, -2.256980353643891447E-27 ) ) ;
#7049=CARTESIAN_POINT ( 'NONE',  ( -4.330127018922234505, -2.775557561562891351E-14, -7.499999999999989342 ) ) ;
#7070=CARTESIAN_POINT ( 'NONE',  ( 4.330127018922095949, 4.689110867544643568, -7.500000000000003553 ) ) ;
#7089=ADVANCED_FACE ( 'NONE', ( #23199 ), #14354, .F. ) ;
#7112=DIRECTION ( 'NONE',  ( 5.551115123561405253E-17, 1.000000000000000000, 2.256980353643891447E-27 ) ) ;
#7163=DIRECTION ( 'NONE',  ( 1.039244538888917269E-16, -0.2588190451025179084, 0.9659258262890690894 ) ) ;
#7173=EDGE_CURVE ( 'NONE', #21697, #4944, #20476, .T. ) ;
#7183=CARTESIAN_POINT ( 'NONE',  ( -5.051814855409253902, 4.882486540518882201, 6.249999999999994671 ) ) ;
#7203=AXIS2_PLACEMENT_3D ( 'NONE', #733, #2600, #21910 ) ;
#7229=VERTEX_POINT ( 'NONE', #8575 ) ;
#7254=CIRCLE ( 'NONE', #20394, 7.499999999999998224 ) ;
#7308=CIRCLE ( 'NONE', #15909, 7.500000000000001776 ) ;
#7361=AXIS2_PLACEMENT_3D ( 'NONE', #9149, #19742, #2194 ) ;
#7389=AXIS2_PLACEMENT_3D ( 'NONE', #22784, #6658, #22321 ) ;
#7442=CARTESIAN_POINT ( 'NONE',  ( -6.938893903907228378E-14, 4.999999999999976907, -4.163336342344337027E-14 ) ) ;
#7443=APPLICATION_CONTEXT ( 'automotive_design' ) ;
#7465=CIRCLE ( 'NONE', #10461, 4.750000000000000000 ) ;
#7469=LINE ( 'NONE', #15922, #9864 ) ;
#7483=VERTEX_POINT ( 'NONE', #1629 ) ;
#7484=ORIENTED_EDGE ( 'NONE', *, *, #12530, .F. ) ;
#7489=LINE ( 'NONE', #14658, #7613 ) ;
#7511=ADVANCED_FACE ( 'NONE', ( #11363 ), #19972, .F. ) ;
#7519=DIRECTION ( 'NONE',  ( -9.693457064947022734E-26, 0.000000000000000000, 1.000000000000000000 ) ) ;
#7533=EDGE_CURVE ( 'NONE', #16514, #10858, #7465, .T. ) ;
#7539=EDGE_CURVE ( 'NONE', #7229, #1035, #21854, .T. ) ;
#7605=CARTESIAN_POINT ( 'NONE',  ( -6.938893903907228378E-14, 4.999999999999976907, -4.163336342344337027E-14 ) ) ;
#7606=LINE ( 'NONE', #5504, #22406 ) ;
#7609=CARTESIAN_POINT ( 'NONE',  ( -3.610629513653773603, 4.785505255291086613, -7.500000000000001776 ) ) ;
#7613=VECTOR ( 'NONE', #21730, 1000.000000000000000 ) ;
#7678=DIRECTION ( 'NONE',  ( -5.551115123561405253E-17, -1.000000000000000000, -2.256980353643891447E-27 ) ) ;
#7713=AXIS2_PLACEMENT_3D ( 'NONE', #22809, #20465, #17027 ) ;
#7727=CARTESIAN_POINT ( 'NONE',  ( -4.330127018922234505, 4.689110867544671102, -7.500000000000000000 ) ) ;
#7756=DIRECTION ( 'NONE',  ( -9.693457064947022734E-26, 0.000000000000000000, 1.000000000000000000 ) ) ;
#7767=SURFACE_STYLE_FILL_AREA ( #9651 ) ;
#7851=CARTESIAN_POINT ( 'NONE',  ( -6.938893903907228378E-14, 4.999999999999976907, -4.163336342344337027E-14 ) ) ;
#7901=DIRECTION ( 'NONE',  ( -0.5000000000000006661, 2.269329254444894332E-16, 0.8660254037844382635 ) ) ;
#7939=ADVANCED_FACE ( 'NONE', ( #20182 ), #4055, .F. ) ;
#7963=CARTESIAN_POINT ( 'NONE',  ( -6.938893903907228378E-14, 0.7368602791855416445, -1.387778780781445676E-14 ) ) ;
#7997=AXIS2_PLACEMENT_3D ( 'NONE', #15780, #16125, #12605 ) ;
#8037=VECTOR ( 'NONE', #9424, 1000.000000000000000 ) ;
#8083=EDGE_CURVE ( 'NONE', #16003, #12006, #6372, .T. ) ;
#8091=B_SPLINE_CURVE_WITH_KNOTS ( 'NONE', 3,
 ( #822, #15158, #4563, #8460 ),
 .UNSPECIFIED., .F., .F.,
 ( 4, 4 ),
 ( 2.309401076293742455E-07, 0.004330357959029834669 ),
 .UNSPECIFIED. ) ;
#8179=ORIENTED_EDGE ( 'NONE', *, *, #23103, .T. ) ;
#8189=CARTESIAN_POINT ( 'NONE',  ( -8.326672684688674053E-14, -1.110223024625156540E-13, 7.500000000000000000 ) ) ;
#8237=EDGE_CURVE ( 'NONE', #20666, #10858, #17129, .T. ) ;
#8240=PLANE ( 'NONE',  #6165 ) ;
#8270=B_SPLINE_CURVE_WITH_KNOTS ( 'NONE', 3,
 ( #9049, #12216, #21539, #7070 ),
 .UNSPECIFIED., .F., .F.,
 ( 4, 4 ),
 ( 0.004330357959029895384, 0.008660484977952097319 ),
 .UNSPECIFIED. ) ;
#8278=B_SPLINE_CURVE_WITH_KNOTS ( 'NONE', 3,
 ( #21873, #8944, #462, #3537 ),
 .UNSPECIFIED., .F., .F.,
 ( 4, 4 ),
 ( 2.309401076647795080E-07, 0.004330357959029895384 ),
 .UNSPECIFIED. ) ;
#8355=CARTESIAN_POINT ( 'NONE',  ( 6.495190528383217199, 0.000000000000000000, -3.750000000000000000 ) ) ;
#8361=DIRECTION ( 'NONE',  ( 1.000000000000000000, -5.551115122690166315E-17, -1.001543066815839268E-16 ) ) ;
#8409=ORIENTED_EDGE ( 'NONE', *, *, #20226, .F. ) ;
#8460=CARTESIAN_POINT ( 'NONE',  ( -6.495190528383335327, 5.000000000000018652, -3.750000000000003553 ) ) ;
#8482=CONICAL_SURFACE ( 'NONE', #7361, 7.500000000000001776, 1.308996938995750092 ) ;
#8538=CARTESIAN_POINT ( 'NONE',  ( -4.330127018922255822, -9.714451465470119729E-14, 7.499999999999985789 ) ) ;
#8575=CARTESIAN_POINT ( 'NONE',  ( 4.330127018922095949, 4.689110867544643568, -7.500000000000003553 ) ) ;
#8582=AXIS2_PLACEMENT_3D ( 'NONE', #3870, #11393, #7756 ) ;
#8601=VERTEX_POINT ( 'NONE', #17306 ) ;
#8604=ORIENTED_EDGE ( 'NONE', *, *, #18330, .T. ) ;
#8639=ORIENTED_EDGE ( 'NONE', *, *, #21320, .T. ) ;
#8788=ORIENTED_EDGE ( 'NONE', *, *, #20327, .F. ) ;
#8815=AXIS2_PLACEMENT_3D ( 'NONE', #10403, #6759, #13822 ) ;
#8819=ADVANCED_FACE ( 'NONE', ( #8967 ), #9150, .T. ) ;
#8825=AXIS2_PLACEMENT_3D ( 'NONE', #13659, #6479, #17402 ) ;
#8830=CARTESIAN_POINT ( 'NONE',  ( 7.270142102516842962E-25, -4.472841332603135502E-27, -7.499999999999998224 ) ) ;
#8845=ORIENTED_EDGE ( 'NONE', *, *, #19046, .T. ) ;
#8914=FACE_OUTER_BOUND ( 'NONE', #2039, .T. ) ;
#8917=FACE_OUTER_BOUND ( 'NONE', #15349, .T. ) ;
#8923=EDGE_CURVE ( 'NONE', #11150, #12860, #16352, .T. ) ;
#8930=AXIS2_PLACEMENT_3D ( 'NONE', #22110, #6002, #20342 ) ;
#8931=VECTOR ( 'NONE', #20215, 1000.000000000000000 ) ;
#8944=CARTESIAN_POINT ( 'NONE',  ( 7.938566201357313723, 4.882486540518877760, -1.249999999999957145 ) ) ;
#8967=FACE_OUTER_BOUND ( 'NONE', #20657, .T. ) ;
#8975=AXIS2_PLACEMENT_3D ( 'NONE', #7851, #11024, #18217 ) ;
#9048=ORIENTED_EDGE ( 'NONE', *, *, #15249, .F. ) ;
#9049=CARTESIAN_POINT ( 'NONE',  ( 6.495190528383244732, 4.999999999999948486, -3.750000000000000000 ) ) ;
#9056=CIRCLE ( 'NONE', #18440, 7.499999999999998224 ) ;
#9078=ADVANCED_FACE ( 'NONE', ( #957 ), #8240, .F. ) ;
#9125=PRODUCT_DEFINITION_CONTEXT ( 'detailed design', #7443, 'design' ) ;
#9139=DIRECTION ( 'NONE',  ( 0.8660254037844387076, -2.506296930348933473E-16, -0.4999999999999998335 ) ) ;
#9149=CARTESIAN_POINT ( 'NONE',  ( -6.938893903907228378E-14, 4.999999999999976907, -4.163336342344337027E-14 ) ) ;
#9150=CONICAL_SURFACE ( 'NONE', #14403, 7.500000000000001776, 1.308996938995750092 ) ;
#9205=B_SPLINE_CURVE_WITH_KNOTS ( 'NONE', 3,
 ( #12780, #20432, #2304, #18542 ),
 .UNSPECIFIED., .F., .F.,
 ( 4, 4 ),
 ( 0.004330357959029864159, 0.008660484977952059155 ),
 .UNSPECIFIED. ) ;
#9208=CIRCLE ( 'NONE', #22360, 7.499999999999998224 ) ;
#9265=LINE ( 'NONE', #13146, #16660 ) ;
#9424=DIRECTION ( 'NONE',  ( 1.000000000000000000, -5.551115122690158919E-17, 1.001543064812511222E-16 ) ) ;
#9471=VERTEX_POINT ( 'NONE', #6100 ) ;
#9502=DIRECTION ( 'NONE',  ( -9.693522803355793065E-26, 5.963788443470849249E-28, 1.000000000000000000 ) ) ;
#9569=ORIENTED_EDGE ( 'NONE', *, *, #18133, .F. ) ;
#9599=ORIENTED_EDGE ( 'NONE', *, *, #1358, .F. ) ;
#9620=ORIENTED_EDGE ( 'NONE', *, *, #10397, .F. ) ;
#9623=DIRECTION ( 'NONE',  ( -5.551115123561405253E-17, -1.000000000000000000, -2.256980353643891447E-27 ) ) ;
#9651=FILL_AREA_STYLE ('',( #16804 ) ) ;
#9676=ORIENTED_EDGE ( 'NONE', *, *, #3742, .F. ) ;
#9708=ADVANCED_FACE ( 'NONE', ( #21842 ), #4172, .F. ) ;
#9786=PRESENTATION_STYLE_ASSIGNMENT (( #1202 ) ) ;
#9806=EDGE_CURVE ( 'NONE', #17095, #12860, #7489, .T. ) ;
#9829=CONICAL_SURFACE ( 'NONE', #10207, 7.500000000000001776, 1.308996938995750092 ) ;
#9864=VECTOR ( 'NONE', #3700, 1000.000000000000000 ) ;
#9883=VECTOR ( 'NONE', #15000, 1000.000000000000227 ) ;
#9896=AXIS2_PLACEMENT_3D ( 'NONE', #18933, #12076, #11864 ) ;
#9911=SURFACE_SIDE_STYLE ('',( #16939 ) ) ;
#9912=ORIENTED_EDGE ( 'NONE', *, *, #21971, .F. ) ;
#9941=EDGE_CURVE ( 'NONE', #18303, #21697, #17225, .T. ) ;
#9952=DIRECTION ( 'NONE',  ( -9.693647360340828445E-26, 0.000000000000000000, 1.000000000000000000 ) ) ;
#9972=ORIENTED_EDGE ( 'NONE', *, *, #8923, .T. ) ;
#9977=ADVANCED_FACE ( 'NONE', ( #11467 ), #117, .F. ) ;
#10010=CARTESIAN_POINT ( 'NONE',  ( -6.938893903907228378E-14, 4.999999999999976907, -4.163336342344337027E-14 ) ) ;
#10092=CARTESIAN_POINT ( 'NONE',  ( -6.495190528383335327, 5.000000000000018652, -3.750000000000003553 ) ) ;
#10132=DIRECTION ( 'NONE',  ( 1.001543066815839268E-16, 2.211965978239706699E-27, 1.000000000000000000 ) ) ;
#10173=VERTEX_POINT ( 'NONE', #3807 ) ;
#10207=AXIS2_PLACEMENT_3D ( 'NONE', #16440, #1554, #7519 ) ;
#10208=FACE_OUTER_BOUND ( 'NONE', #20686, .T. ) ;
#10213=ORIENTED_EDGE ( 'NONE', *, *, #3881, .T. ) ;
#10230=DIRECTION ( 'NONE',  ( -5.551115123561405253E-17, -1.000000000000000000, -2.256980353643891447E-27 ) ) ;
#10261=DIRECTION ( 'NONE',  ( -5.551115123561405253E-17, -1.000000000000000000, -2.256980353643891447E-27 ) ) ;
#10390=CARTESIAN_POINT ( 'NONE',  ( 8.660254037844344666, -2.775557561562891351E-14, 2.081668171172168513E-14 ) ) ;
#10397=EDGE_CURVE ( 'NONE', #17574, #4163, #18349, .T. ) ;
#10398=ORIENTED_EDGE ( 'NONE', *, *, #18187, .T. ) ;
#10403=CARTESIAN_POINT ( 'NONE',  ( -6.938893903907228378E-14, 4.999999999999976907, -4.163336342344337027E-14 ) ) ;
#10415=CARTESIAN_POINT ( 'NONE',  ( -8.660254037844421049, 4.999999999999948486, -1.387778780781445676E-14 ) ) ;
#10420=EDGE_CURVE ( 'NONE', #20563, #7229, #8270, .T. ) ;
#10440=AXIS2_PLACEMENT_3D ( 'NONE', #507, #7678, #5910 ) ;
#10461=AXIS2_PLACEMENT_3D ( 'NONE', #7963, #21750, #14670 ) ;
#10494=FACE_OUTER_BOUND ( 'NONE', #17481, .T. ) ;
#10525=ORIENTED_EDGE ( 'NONE', *, *, #7533, .T. ) ;
#10690=ORIENTED_EDGE ( 'NONE', *, *, #3881, .F. ) ;
#10747=ORIENTED_EDGE ( 'NONE', *, *, #15249, .T. ) ;
#10772=VECTOR ( 'NONE', #14278, 1000.000000000000000 ) ;
#10858=VERTEX_POINT ( 'NONE', #5028 ) ;
#10884=COLOUR_RGB ( '', 0.40784314, 0.44705882, 0.49803922) ;
#10954=AXIS2_PLACEMENT_3D ( 'NONE', #7605, #11249, #672 ) ;
#10994=DIRECTION ( 'NONE',  ( -9.693522803355793065E-26, 5.963788443470849249E-28, 1.000000000000000000 ) ) ;
#11024=DIRECTION ( 'NONE',  ( -5.551115123561405253E-17, -1.000000000000000000, -2.256980353643891447E-27 ) ) ;
#11029=ORIENTED_EDGE ( 'NONE', *, *, #9941, .F. ) ;
#11099=EDGE_CURVE ( 'NONE', #4944, #11150, #16757, .T. ) ;
#11122=ORIENTED_EDGE ( 'NONE', *, *, #14439, .F. ) ;
#11146=APPLICATION_CONTEXT ( 'automotive_design' ) ;
#11150=VERTEX_POINT ( 'NONE', #8189 ) ;
#11223=CARTESIAN_POINT ( 'NONE',  ( 0.000000000000000000, 0.000000000000000000, 0.000000000000000000 ) ) ;
#11229=CARTESIAN_POINT ( 'NONE',  ( -4.330127018922248716, 4.689110867544532546, 7.500000000000007105 ) ) ;
#11234=AXIS2_PLACEMENT_3D ( 'NONE', #16289, #3818, #10994 ) ;
#11249=DIRECTION ( 'NONE',  ( -5.551115123561405253E-17, -1.000000000000000000, -2.256980353643891447E-27 ) ) ;
#11308=ORIENTED_EDGE ( 'NONE', *, *, #2498, .T. ) ;
#11310=CIRCLE ( 'NONE', #7203, 7.500000000000001776 ) ;
#11363=FACE_OUTER_BOUND ( 'NONE', #6242, .T. ) ;
#11393=DIRECTION ( 'NONE',  ( -5.551115123561405253E-17, -1.000000000000000000, -2.256980353643891447E-27 ) ) ;
#11444=DIRECTION ( 'NONE',  ( -9.693522803355793065E-26, 5.963788443470849249E-28, 1.000000000000000000 ) ) ;
#11467=FACE_OUTER_BOUND ( 'NONE', #11781, .T. ) ;
#11508=CARTESIAN_POINT ( 'NONE',  ( -8.660254037844406838, 0.000000000000000000, 6.938893903907228378E-15 ) ) ;
#11542=FILL_AREA_STYLE_COLOUR ( '', #10884 ) ;
#11557=VERTEX_POINT ( 'NONE', #19436 ) ;
#11581=CONICAL_SURFACE ( 'NONE', #8582, 7.500000000000001776, 1.308996938995750092 ) ;
#11596=CARTESIAN_POINT ( 'NONE',  ( 1.446367150925043532, 4.999999999999985789, -7.500000000000003553 ) ) ;
#11701=ORIENTED_EDGE ( 'NONE', *, *, #7533, .F. ) ;
#11730=CARTESIAN_POINT ( 'NONE',  ( 0.000000000000000000, 0.000000000000000000, 0.000000000000000000 ) ) ;
#11781=EDGE_LOOP ( 'NONE', ( #21180, #21923, #19221, #3486, #21695, #5011 ) ) ;
#11796=DIRECTION ( 'NONE',  ( 9.693647360340828445E-26, 0.000000000000000000, -1.000000000000000000 ) ) ;
#11816=ORIENTED_EDGE ( 'NONE', *, *, #16907, .T. ) ;
#11845=ORIENTED_EDGE ( 'NONE', *, *, #8083, .T. ) ;
#11861=DIRECTION ( 'NONE',  ( -5.551115123561405253E-17, -1.000000000000000000, -2.256980353643891447E-27 ) ) ;
#11864=DIRECTION ( 'NONE',  ( -9.693522803355793065E-26, 5.963788443470849249E-28, 1.000000000000000000 ) ) ;
#11885=CARTESIAN_POINT ( 'NONE',  ( -4.330127018922179438, 4.999999999999976907, -7.500000000000000000 ) ) ;
#11936=DIRECTION ( 'NONE',  ( -5.551115123561405253E-17, -1.000000000000000000, -2.256980353643891447E-27 ) ) ;
#11943=PLANE ( 'NONE',  #7389 ) ;
#11992=DIRECTION ( 'NONE',  ( -1.436734306171084565E-17, -0.2588190451025179084, -0.9659258262890690894 ) ) ;
#12003=( GEOMETRIC_REPRESENTATION_CONTEXT ( 3 ) GLOBAL_UNCERTAINTY_ASSIGNED_CONTEXT ( ( #18760 ) ) GLOBAL_UNIT_ASSIGNED_CONTEXT ( ( #20735, #22499, #6386 ) ) REPRESENTATION_CONTEXT ( 'NONE', 'WORKASPACE' ) );
#12006=VERTEX_POINT ( 'NONE', #10092 ) ;
#12029=EDGE_LOOP ( 'NONE', ( #21786, #1002, #11029 ) ) ;
#12036=VERTEX_POINT ( 'NONE', #22334 ) ;
#12046=CIRCLE ( 'NONE', #2287, 7.500000000000001776 ) ;
#12072=DIRECTION ( 'NONE',  ( -5.551115123561405253E-17, -1.000000000000000000, -2.256980353643891447E-27 ) ) ;
#12076=DIRECTION ( 'NONE',  ( 5.551115123561405253E-17, 1.000000000000000000, -5.963788443470795439E-28 ) ) ;
#12112=AXIS2_PLACEMENT_3D ( 'NONE', #11223, #3927, #11444 ) ;
#12216=CARTESIAN_POINT ( 'NONE',  ( 5.773502691896191585, 4.999999999999984901, -4.999999999999999112 ) ) ;
#12240=DIRECTION ( 'NONE',  ( -1.000000000000000000, 5.551115122690166315E-17, 1.001543066815839268E-16 ) ) ;
#12429=CARTESIAN_POINT ( 'NONE',  ( 0.000000000000000000, 0.000000000000000000, 0.000000000000000000 ) ) ;
#12448=ORIENTED_EDGE ( 'NONE', *, *, #16709, .T. ) ;
#12455=CONICAL_SURFACE ( 'NONE', #5332, 7.500000000000001776, 1.308996938995750092 ) ;
#12506=ORIENTED_EDGE ( 'NONE', *, *, #16907, .F. ) ;
#12530=EDGE_CURVE ( 'NONE', #11557, #20666, #5819, .T. ) ;
#12590=AXIS2_PLACEMENT_3D ( 'NONE', #3400, #12072, #5662 ) ;
#12605=DIRECTION ( 'NONE',  ( -9.693457064947022734E-26, 0.000000000000000000, 1.000000000000000000 ) ) ;
#12673=CARTESIAN_POINT ( 'NONE',  ( -7.216878364870350282, 4.999999999999984901, 2.499999999999995115 ) ) ;
#12674=EDGE_CURVE ( 'NONE', #17239, #9471, #2407, .T. ) ;
#12780=CARTESIAN_POINT ( 'NONE',  ( 6.495190528383244732, 4.999999999999935163, 3.750000000000003553 ) ) ;
#12796=EDGE_LOOP ( 'NONE', ( #9599, #15575, #13502 ) ) ;
#12828=VECTOR ( 'NONE', #11936, 1000.000000000000000 ) ;
#12842=CARTESIAN_POINT ( 'NONE',  ( -2.886699270652946403, 4.864326267994410813, 7.500000000000007105 ) ) ;
#12852=DIRECTION ( 'NONE',  ( -1.000000000000000000, 5.551115122690158919E-17, -1.001543064812511222E-16 ) ) ;
#12860=VERTEX_POINT ( 'NONE', #4373 ) ;
#12964=CARTESIAN_POINT ( 'NONE',  ( -3.610629513653814016, 4.785505255291060855, 7.500000000000006217 ) ) ;
#12971=DIRECTION ( 'NONE',  ( -0.8660254037844382635, -1.951185418111810735E-16, -0.5000000000000006661 ) ) ;
#13118=MANIFOLD_SOLID_BREP ( 'Cut-Extrude2', #15564 ) ;
#13136=ORIENTED_EDGE ( 'NONE', *, *, #21971, .T. ) ;
#13146=CARTESIAN_POINT ( 'NONE',  ( 4.330127018922110160, -5.551115123125782702E-14, -7.499999999999996447 ) ) ;
#13240=CARTESIAN_POINT ( 'NONE',  ( -6.938893903907228378E-14, 4.999999999999976907, -4.163336342344337027E-14 ) ) ;
#13319=CARTESIAN_POINT ( 'NONE',  ( 1.446367150925026657, 4.999999999999964473, 7.500000000000007105 ) ) ;
#13330=ORIENTED_EDGE ( 'NONE', *, *, #10397, .T. ) ;
#13390=B_SPLINE_CURVE_WITH_KNOTS ( 'NONE', 3,
 ( #16762, #3959, #2200, #438, #7609, #7727 ),
 .UNSPECIFIED., .F., .F.,
 ( 4, 2, 4 ),
 ( 0.02095135962594951370, 0.02312341562515501936, 0.02529547162436052155 ),
 .UNSPECIFIED. ) ;
#13403=DIRECTION ( 'NONE',  ( -5.551115123561405253E-17, -1.000000000000000000, -2.256980353643891447E-27 ) ) ;
#13430=DIRECTION ( 'NONE',  ( -5.551115123561405253E-17, -1.000000000000000000, -2.256980353643891447E-27 ) ) ;
#13456=VECTOR ( 'NONE', #18692, 1000.000000000000227 ) ;
#13502=ORIENTED_EDGE ( 'NONE', *, *, #18856, .F. ) ;
#13522=DIRECTION ( 'NONE',  ( 5.551115123561405253E-17, 1.000000000000000000, 2.256980353643891447E-27 ) ) ;
#13659=CARTESIAN_POINT ( 'NONE',  ( -6.938893903907228378E-14, 4.999999999999976907, -4.163336342344337027E-14 ) ) ;
#13681=AXIS2_PLACEMENT_3D ( 'NONE', #13240, #20424, #9952 ) ;
#13685=LINE ( 'NONE', #22858, #4723 ) ;
#13694=CARTESIAN_POINT ( 'NONE',  ( 8.660254037844344666, -2.775557561562891351E-14, 2.081668171172168513E-14 ) ) ;
#13822=DIRECTION ( 'NONE',  ( -9.693457064947022734E-26, 0.000000000000000000, 1.000000000000000000 ) ) ;
#13899=ORIENTED_EDGE ( 'NONE', *, *, #22962, .T. ) ;
#13920=ORIENTED_EDGE ( 'NONE', *, *, #19458, .T. ) ;
#13928=ORIENTED_EDGE ( 'NONE', *, *, #16709, .F. ) ;
#14049=ORIENTED_EDGE ( 'NONE', *, *, #12530, .T. ) ;
#14052=ORIENTED_EDGE ( 'NONE', *, *, #15119, .F. ) ;
#14115=ORIENTED_EDGE ( 'NONE', *, *, #14703, .T. ) ;
#14227=VECTOR ( 'NONE', #3966, 1000.000000000000000 ) ;
#14278=DIRECTION ( 'NONE',  ( -0.4999999999999999445, -4.767331059895059913E-16, -0.8660254037844387076 ) ) ;
#14283=EDGE_LOOP ( 'NONE', ( #13920, #13899, #4245 ) ) ;
#14354=PLANE ( 'NONE',  #5568 ) ;
#14403=AXIS2_PLACEMENT_3D ( 'NONE', #19667, #6981, #18131 ) ;
#14408=EDGE_CURVE ( 'NONE', #9471, #20563, #12046, .T. ) ;
#14419=CARTESIAN_POINT ( 'NONE',  ( 2.889332061078579539, 4.882140790251119356, 7.500000000000007105 ) ) ;
#14439=EDGE_CURVE ( 'NONE', #16514, #10173, #3420, .T. ) ;
#14462=ORIENTED_EDGE ( 'NONE', *, *, #10420, .T. ) ;
#14506=VERTEX_POINT ( 'NONE', #8355 ) ;
#14541=EDGE_CURVE ( 'NONE', #12036, #10173, #9056, .T. ) ;
#14562=CIRCLE ( 'NONE', #10440, 7.499999999999998224 ) ;
#14624=AXIS2_PLACEMENT_3D ( 'NONE', #5520, #16664, #5984 ) ;
#14639=PLANE ( 'NONE',  #12112 ) ;
#14651=ORIENTED_EDGE ( 'NONE', *, *, #16585, .T. ) ;
#14658=CARTESIAN_POINT ( 'NONE',  ( 4.330127018922103055, 4.999999999999838352, 7.499999999999971578 ) ) ;
#14670=DIRECTION ( 'NONE',  ( 9.693647360340828445E-26, 0.000000000000000000, -1.000000000000000000 ) ) ;
#14703=EDGE_CURVE ( 'NONE', #23120, #20563, #8278, .T. ) ;
#14778=CARTESIAN_POINT ( 'NONE',  ( -4.330127018922255822, -9.714451465470119729E-14, 7.499999999999985789 ) ) ;
#14813=AXIS2_PLACEMENT_3D ( 'NONE', #22374, #10132, #8361 ) ;
#14942=SURFACE_SIDE_STYLE ('',( #7767 ) ) ;
#14950=CARTESIAN_POINT ( 'NONE',  ( -4.330127018922248716, 4.689110867544532546, 7.500000000000007105 ) ) ;
#15000=DIRECTION ( 'NONE',  ( 0.4999999999999997780, 5.044886816051349048E-16, 0.8660254037844387076 ) ) ;
#15043=ORIENTED_EDGE ( 'NONE', *, *, #20821, .F. ) ;
#15087=ADVANCED_FACE ( 'NONE', ( #8914 ), #21120, .T. ) ;
#15119=EDGE_CURVE ( 'NONE', #12006, #7483, #17258, .T. ) ;
#15150=( GEOMETRIC_REPRESENTATION_CONTEXT ( 3 ) GLOBAL_UNCERTAINTY_ASSIGNED_CONTEXT ( ( #5579 ) ) GLOBAL_UNIT_ASSIGNED_CONTEXT ( ( #6129, #6015, #6366 ) ) REPRESENTATION_CONTEXT ( 'NONE', 'WORKASPACE' ) );
#15158=CARTESIAN_POINT ( 'NONE',  ( -5.051814855409225480, 4.882486540518908846, -6.249999999999975131 ) ) ;
#15170=ORIENTED_EDGE ( 'NONE', *, *, #19046, .F. ) ;
#15175=DIRECTION ( 'NONE',  ( 5.551115123561405253E-17, 1.000000000000000000, 2.256980353643891447E-27 ) ) ;
#15177=CARTESIAN_POINT ( 'NONE',  ( -8.326672684688674053E-14, 4.999999999999893419, 7.499999999999958256 ) ) ;
#15221=ORIENTED_EDGE ( 'NONE', *, *, #14408, .T. ) ;
#15226=ADVANCED_FACE ( 'NONE', ( #21129 ), #12455, .T. ) ;
#15249=EDGE_CURVE ( 'NONE', #7483, #18303, #3132, .T. ) ;
#15282=DIRECTION ( 'NONE',  ( -9.693522803355793065E-26, 5.963788443470849249E-28, 1.000000000000000000 ) ) ;
#15286=VERTEX_POINT ( 'NONE', #4657 ) ;
#15293=FACE_OUTER_BOUND ( 'NONE', #16639, .T. ) ;
#15349=EDGE_LOOP ( 'NONE', ( #10525, #17517, #12448, #8179, #15486, #11122 ) ) ;
#15421=ORIENTED_EDGE ( 'NONE', *, *, #1399, .F. ) ;
#15460=DIRECTION ( 'NONE',  ( 9.693522803355793065E-26, -5.963788443470848352E-28, -1.000000000000000000 ) ) ;
#15486=ORIENTED_EDGE ( 'NONE', *, *, #14541, .T. ) ;
#15525=CYLINDRICAL_SURFACE ( 'NONE', #8825, 4.750000000000000000 ) ;
#15540=ORIENTED_EDGE ( 'NONE', *, *, #10420, .F. ) ;
#15564=CLOSED_SHELL ( 'NONE', ( #20479, #7511, #15848, #15688, #9078, #7939, #16722, #18792, #22107, #6765, #7089, #18429, #21616, #9708, #3356, #19875, #15226, #15743, #4810, #8819, #15087, #5963, #9977 ) ) ;
#15575=ORIENTED_EDGE ( 'NONE', *, *, #14541, .F. ) ;
#15688=ADVANCED_FACE ( 'NONE', ( #18222 ), #18443, .F. ) ;
#15743=ADVANCED_FACE ( 'NONE', ( #19672 ), #9829, .T. ) ;
#15780=CARTESIAN_POINT ( 'NONE',  ( -6.938893903907228378E-14, 4.999999999999976907, -4.163336342344337027E-14 ) ) ;
#15808=CARTESIAN_POINT ( 'NONE',  ( -6.495190528383341544, 4.999999999999920952, 3.750000000000017319 ) ) ;
#15841=AXIS2_PLACEMENT_3D ( 'NONE', #12429, #19612, #2071 ) ;
#15848=ADVANCED_FACE ( 'NONE', ( #10494 ), #17662, .F. ) ;
#15890=DIRECTION ( 'NONE',  ( 0.5000000000000006661, -2.269329254444893839E-16, -0.8660254037844382635 ) ) ;
#15909=AXIS2_PLACEMENT_3D ( 'NONE', #7442, #7112, #21800 ) ;
#15914=ORIENTED_EDGE ( 'NONE', *, *, #7173, .T. ) ;
#15922=CARTESIAN_POINT ( 'NONE',  ( -6.938893903861184144E-14, 4.999999999999976907, -4.750000000000041744 ) ) ;
#16003=VERTEX_POINT ( 'NONE', #19256 ) ;
#16055=ORIENTED_EDGE ( 'NONE', *, *, #1358, .T. ) ;
#16125=DIRECTION ( 'NONE',  ( 5.551115123561405253E-17, 1.000000000000000000, 2.256980353643891447E-27 ) ) ;
#16133=PRODUCT_DEFINITION_FORMATION_WITH_SPECIFIED_SOURCE ( 'ANY', '', #21350, .NOT_KNOWN. ) ;
#16219=EDGE_LOOP ( 'NONE', ( #2414, #8409, #15170 ) ) ;
#16231=EDGE_CURVE ( 'NONE', #8601, #11150, #16963, .T. ) ;
#16261=CIRCLE ( 'NONE', #7997, 7.500000000000001776 ) ;
#16289=CARTESIAN_POINT ( 'NONE',  ( 0.000000000000000000, 0.000000000000000000, 0.000000000000000000 ) ) ;
#16350=ORIENTED_EDGE ( 'NONE', *, *, #9806, .T. ) ;
#16352=LINE ( 'NONE', #252, #8037 ) ;
#16381=ORIENTED_EDGE ( 'NONE', *, *, #21320, .F. ) ;
#16440=CARTESIAN_POINT ( 'NONE',  ( -6.938893903907228378E-14, 4.999999999999976907, -4.163336342344337027E-14 ) ) ;
#16514=VERTEX_POINT ( 'NONE', #3368 ) ;
#16532=DIRECTION ( 'NONE',  ( -1.000000000000000000, 5.551115122690166315E-17, 1.001543066815839268E-16 ) ) ;
#16585=EDGE_CURVE ( 'NONE', #11557, #16514, #7469, .T. ) ;
#16594=ORIENTED_EDGE ( 'NONE', *, *, #11099, .T. ) ;
#16639=EDGE_LOOP ( 'NONE', ( #2850, #18526, #14651, #20966 ) ) ;
#16657=LINE ( 'NONE', #16767, #8931 ) ;
#16660=VECTOR ( 'NONE', #16532, 1000.000000000000000 ) ;
#16664=DIRECTION ( 'NONE',  ( 5.551115123561405253E-17, 1.000000000000000000, 2.256980353643891447E-27 ) ) ;
#16699=CARTESIAN_POINT ( 'NONE',  ( 4.330127018922110160, 4.689110867544560080, 7.499999999999985789 ) ) ;
#16709=EDGE_CURVE ( 'NONE', #11150, #21697, #7254, .T. ) ;
#16722=ADVANCED_FACE ( 'NONE', ( #18629 ), #14639, .F. ) ;
#16750=EDGE_CURVE ( 'NONE', #10858, #16514, #3118, .T. ) ;
#16757=LINE ( 'NONE', #14778, #21887 ) ;
#16762=CARTESIAN_POINT ( 'NONE',  ( -4.857225732735059864E-14, 4.999999999999976907, -7.500000000000003553 ) ) ;
#16767=CARTESIAN_POINT ( 'NONE',  ( 8.660254037844344666, -2.775557561562891351E-14, 2.081668171172168513E-14 ) ) ;
#16794=ORIENTED_EDGE ( 'NONE', *, *, #7539, .T. ) ;
#16804=FILL_AREA_STYLE_COLOUR ( '', #20820 ) ;
#16821=FACE_OUTER_BOUND ( 'NONE', #2415, .T. ) ;
#16845=B_SPLINE_CURVE_WITH_KNOTS ( 'NONE', 3,
 ( #19385, #5511, #12673, #19859 ),
 .UNSPECIFIED., .F., .F.,
 ( 4, 4 ),
 ( 2.309401076552564490E-07, 0.004330357959029877170 ),
 .UNSPECIFIED. ) ;
#16891=ORIENTED_EDGE ( 'NONE', *, *, #2498, .F. ) ;
#16907=EDGE_CURVE ( 'NONE', #12006, #17574, #16261, .T. ) ;
#16910=PLANE ( 'NONE',  #8930 ) ;
#16925=ORIENTED_EDGE ( 'NONE', *, *, #1399, .T. ) ;
#16939=SURFACE_STYLE_FILL_AREA ( #4599 ) ;
#16963=CIRCLE ( 'NONE', #15841, 7.499999999999998224 ) ;
#17027=DIRECTION ( 'NONE',  ( 9.693522803355793065E-26, -5.963788443470848352E-28, -1.000000000000000000 ) ) ;
#17048=VECTOR ( 'NONE', #13430, 1000.000000000000000 ) ;
#17095=VERTEX_POINT ( 'NONE', #16699 ) ;
#17129=LINE ( 'NONE', #20453, #18128 ) ;
#17153=VECTOR ( 'NONE', #12240, 1000.000000000000000 ) ;
#17160=DIRECTION ( 'NONE',  ( 5.551115123561405253E-17, 1.000000000000000000, -5.963788443470795439E-28 ) ) ;
#17172=FACE_OUTER_BOUND ( 'NONE', #18171, .T. ) ;
#17184=SHAPE_REPRESENTATION_RELATIONSHIP ( 'NONE' , 'NONE' ,  #17992, #2433 ) ;
#17199=DIRECTION ( 'NONE',  ( 5.551115123561405253E-17, 1.000000000000000000, 2.256980353643891447E-27 ) ) ;
#17225=LINE ( 'NONE', #4405, #9883 ) ;
#17239=VERTEX_POINT ( 'NONE', #15177 ) ;
#17258=B_SPLINE_CURVE_WITH_KNOTS ( 'NONE', 3,
 ( #18543, #2425, #22313, #20315 ),
 .UNSPECIFIED., .F., .F.,
 ( 4, 4 ),
 ( 0.004330357959029834669, 0.008660484977952034868 ),
 .UNSPECIFIED. ) ;
#17306=CARTESIAN_POINT ( 'NONE',  ( 6.495190528383258943, -8.326672684688674053E-14, 3.749999999999961808 ) ) ;
#17399=DIRECTION ( 'NONE',  ( 9.693522803355793065E-26, -5.963788443470848352E-28, -1.000000000000000000 ) ) ;
#17402=DIRECTION ( 'NONE',  ( 9.693647360340828445E-26, 0.000000000000000000, -1.000000000000000000 ) ) ;
#17440=DIRECTION ( 'NONE',  ( 0.5000000000000006661, -2.269329254444893839E-16, -0.8660254037844382635 ) ) ;
#17446=CARTESIAN_POINT ( 'NONE',  ( 5.051814855409131333, 4.882486540518882201, 6.249999999999979572 ) ) ;
#17463=ORIENTED_EDGE ( 'NONE', *, *, #7173, .F. ) ;
#17481=EDGE_LOOP ( 'NONE', ( #3239, #22436, #15421 ) ) ;
#17517=ORIENTED_EDGE ( 'NONE', *, *, #4901, .T. ) ;
#17557=AXIS2_PLACEMENT_3D ( 'NONE', #22136, #12971, #7901 ) ;
#17574=VERTEX_POINT ( 'NONE', #15808 ) ;
#17662=PLANE ( 'NONE',  #4562 ) ;
#17664=CARTESIAN_POINT ( 'NONE',  ( 4.330127018922110160, -5.551115123125782702E-14, -7.499999999999996447 ) ) ;
#17894=CARTESIAN_POINT ( 'NONE',  ( 8.660254037844337560, 4.999999999999948486, 2.775557561562891351E-14 ) ) ;
#17992=SHAPE_REPRESENTATION ( 'Lock nut', ( #22115 ), #12003 ) ;
#18047=ORIENTED_EDGE ( 'NONE', *, *, #14703, .F. ) ;
#18120=ORIENTED_EDGE ( 'NONE', *, *, #12674, .T. ) ;
#18128=VECTOR ( 'NONE', #9623, 1000.000000000000000 ) ;
#18129=ORIENTED_EDGE ( 'NONE', *, *, #6067, .F. ) ;
#18131=DIRECTION ( 'NONE',  ( -9.693457064947022734E-26, 0.000000000000000000, 1.000000000000000000 ) ) ;
#18133=EDGE_CURVE ( 'NONE', #17574, #17239, #7308, .T. ) ;
#18154=CARTESIAN_POINT ( 'NONE',  ( 6.495190528383244732, 4.999999999999935163, 3.750000000000003553 ) ) ;
#18171=EDGE_LOOP ( 'NONE', ( #10690, #16794, #8845, #16055, #5549, #9676 ) ) ;
#18187=EDGE_CURVE ( 'NONE', #4163, #17239, #5354, .T. ) ;
#18217=DIRECTION ( 'NONE',  ( 9.693647360340828445E-26, 0.000000000000000000, -1.000000000000000000 ) ) ;
#18222=FACE_OUTER_BOUND ( 'NONE', #20839, .T. ) ;
#18303=VERTEX_POINT ( 'NONE', #20609 ) ;
#18330=EDGE_CURVE ( 'NONE', #3791, #15286, #19068, .T. ) ;
#18349=B_SPLINE_CURVE_WITH_KNOTS ( 'NONE', 3,
 ( #2506, #5177, #7183, #22954 ),
 .UNSPECIFIED., .F., .F.,
 ( 4, 4 ),
 ( 0.004330357959029877170, 0.008660484977952064359 ),
 .UNSPECIFIED. ) ;
#18359=AXIS2_PLACEMENT_3D ( 'NONE', #1290, #13522, #22701 ) ;
#18415=EDGE_LOOP ( 'NONE', ( #2291, #8604, #632, #5050, #9048, #14052 ) ) ;
#18429=ADVANCED_FACE ( 'NONE', ( #17172 ), #1315, .F. ) ;
#18440=AXIS2_PLACEMENT_3D ( 'NONE', #4823, #10230, #17399 ) ;
#18443=PLANE ( 'NONE',  #6459 ) ;
#18509=AXIS2_PLACEMENT_3D ( 'NONE', #2069, #9139, #4068 ) ;
#18526=ORIENTED_EDGE ( 'NONE', *, *, #6067, .T. ) ;
#18527=AXIS2_PLACEMENT_3D ( 'NONE', #20784, #4647, #15460 ) ;
#18542=CARTESIAN_POINT ( 'NONE',  ( 8.660254037844413944, 4.689110867544616035, 2.775557561562891351E-14 ) ) ;
#18543=CARTESIAN_POINT ( 'NONE',  ( -6.495190528383335327, 5.000000000000018652, -3.750000000000003553 ) ) ;
#18590=ORIENTED_EDGE ( 'NONE', *, *, #11099, .F. ) ;
#18615=( LENGTH_UNIT ( ) NAMED_UNIT ( * ) SI_UNIT ( .MILLI., .METRE. ) );
#18629=FACE_OUTER_BOUND ( 'NONE', #12029, .T. ) ;
#18692=DIRECTION ( 'NONE',  ( 0.4999999999999997780, 5.044886816051349048E-16, 0.8660254037844387076 ) ) ;
#18696=EDGE_CURVE ( 'NONE', #3791, #12006, #8091, .T. ) ;
#18727=( NAMED_UNIT ( * ) PLANE_ANGLE_UNIT ( ) SI_UNIT ( $, .RADIAN. ) );
#18760=UNCERTAINTY_MEASURE_WITH_UNIT (LENGTH_MEASURE( 1.000000000000000082E-05 ), #20735, 'distance_accuracy_value', 'NONE');
#18792=ADVANCED_FACE ( 'NONE', ( #4909, #10208 ), #20701, .T. ) ;
#18824=SURFACE_STYLE_USAGE ( .BOTH. , #14942 ) ;
#18856=EDGE_CURVE ( 'NONE', #15286, #12036, #1625, .T. ) ;
#18933=CARTESIAN_POINT ( 'NONE',  ( -6.938893903907228378E-14, 4.999999999999976907, -4.163336342344337027E-14 ) ) ;
#18944=ORIENTED_EDGE ( 'NONE', *, *, #21250, .T. ) ;
#19046=EDGE_CURVE ( 'NONE', #1035, #10173, #9265, .T. ) ;
#19068=LINE ( 'NONE', #11885, #17048 ) ;
#19088=LINE ( 'NONE', #2979, #21652 ) ;
#19196=VECTOR ( 'NONE', #11992, 1000.000000000000000 ) ;
#19216=ORIENTED_EDGE ( 'NONE', *, *, #5369, .F. ) ;
#19220=EDGE_LOOP ( 'NONE', ( #20354, #19876, #16594, #9972, #6267, #4399 ) ) ;
#19221=ORIENTED_EDGE ( 'NONE', *, *, #14439, .T. ) ;
#19236=CARTESIAN_POINT ( 'NONE',  ( 4.330127018922095949, 4.689110867544643568, -7.500000000000003553 ) ) ;
#19256=CARTESIAN_POINT ( 'NONE',  ( -4.857225732735059864E-14, 4.999999999999976907, -7.500000000000003553 ) ) ;
#19385=CARTESIAN_POINT ( 'NONE',  ( -8.660254037844428154, 4.689110867544629357, -1.387778780781445676E-14 ) ) ;
#19436=CARTESIAN_POINT ( 'NONE',  ( -6.950726493550218217E-14, 4.999999999999976907, -4.750000000000041744 ) ) ;
#19458=EDGE_CURVE ( 'NONE', #17239, #17095, #1940, .T. ) ;
#19612=DIRECTION ( 'NONE',  ( -5.551115123561405253E-17, -1.000000000000000000, -2.256980353643891447E-27 ) ) ;
#19667=CARTESIAN_POINT ( 'NONE',  ( -6.938893903907228378E-14, 4.999999999999976907, -4.163336342344337027E-14 ) ) ;
#19672=FACE_OUTER_BOUND ( 'NONE', #3686, .T. ) ;
#19742=DIRECTION ( 'NONE',  ( -5.551115123561405253E-17, -1.000000000000000000, -2.256980353643891447E-27 ) ) ;
#19803=FACE_OUTER_BOUND ( 'NONE', #19220, .T. ) ;
#19820=CIRCLE ( 'NONE', #18359, 4.750000000000000000 ) ;
#19859=CARTESIAN_POINT ( 'NONE',  ( -6.495190528383341544, 4.999999999999920952, 3.750000000000017319 ) ) ;
#19875=ADVANCED_FACE ( 'NONE', ( #15293 ), #15525, .F. ) ;
#19876=ORIENTED_EDGE ( 'NONE', *, *, #1496, .T. ) ;
#19972=CYLINDRICAL_SURFACE ( 'NONE', #8975, 4.750000000000000000 ) ;
#20033=CARTESIAN_POINT ( 'NONE',  ( -4.330127018922199866, 4.999999999999920952, 7.500000000000007105 ) ) ;
#20182=FACE_OUTER_BOUND ( 'NONE', #12796, .T. ) ;
#20202=DIRECTION ( 'NONE',  ( 1.000000000000000000, -5.551115122690158919E-17, 1.001543064812511222E-16 ) ) ;
#20215=DIRECTION ( 'NONE',  ( -0.4999999999999999445, -4.767331059895059913E-16, -0.8660254037844387076 ) ) ;
#20226=EDGE_CURVE ( 'NONE', #10173, #14506, #9208, .T. ) ;
#20282=ORIENTED_EDGE ( 'NONE', *, *, #22962, .F. ) ;
#20315=CARTESIAN_POINT ( 'NONE',  ( -8.660254037844428154, 4.689110867544629357, -1.387778780781445676E-14 ) ) ;
#20327=EDGE_CURVE ( 'NONE', #14506, #8601, #953, .T. ) ;
#20342=DIRECTION ( 'NONE',  ( -9.693522803355793065E-26, 5.963788443470849249E-28, 1.000000000000000000 ) ) ;
#20354=ORIENTED_EDGE ( 'NONE', *, *, #18187, .F. ) ;
#20361=DIRECTION ( 'NONE',  ( -9.693457064947022734E-26, 0.000000000000000000, 1.000000000000000000 ) ) ;
#20367=CARTESIAN_POINT ( 'NONE',  ( -0.7206956945560699657, 4.999999999999962697, 7.500000000000007994 ) ) ;
#20394=AXIS2_PLACEMENT_3D ( 'NONE', #21823, #22165, #6049 ) ;
#20424=DIRECTION ( 'NONE',  ( 5.551115123561405253E-17, 1.000000000000000000, 2.256980353643891447E-27 ) ) ;
#20432=CARTESIAN_POINT ( 'NONE',  ( 7.216878364870232154, 4.999999999999980460, 2.499999999999973355 ) ) ;
#20453=CARTESIAN_POINT ( 'NONE',  ( -6.880723180993772785E-14, 4.999999999999976907, 4.749999999999958256 ) ) ;
#20465=DIRECTION ( 'NONE',  ( -5.551115123561405253E-17, -1.000000000000000000, -2.256980353643891447E-27 ) ) ;
#20467=FACE_OUTER_BOUND ( 'NONE', #2645, .T. ) ;
#20476=LINE ( 'NONE', #11508, #13456 ) ;
#20479=ADVANCED_FACE ( 'NONE', ( #8917 ), #22744, .F. ) ;
#20501=CARTESIAN_POINT ( 'NONE',  ( 4.330127018922110160, 4.689110867544560080, 7.499999999999985789 ) ) ;
#20563=VERTEX_POINT ( 'NONE', #3836 ) ;
#20609=CARTESIAN_POINT ( 'NONE',  ( -8.660254037844406838, 0.000000000000000000, 6.938893903907228378E-15 ) ) ;
#20657=EDGE_LOOP ( 'NONE', ( #14462, #10213, #15043 ) ) ;
#20666=VERTEX_POINT ( 'NONE', #6553 ) ;
#20686=EDGE_LOOP ( 'NONE', ( #21585, #18120, #15221, #2612, #11845, #11816 ) ) ;
#20701=PLANE ( 'NONE',  #9896 ) ;
#20712=CARTESIAN_POINT ( 'NONE',  ( 0.000000000000000000, 0.000000000000000000, 0.000000000000000000 ) ) ;
#20735=( LENGTH_UNIT ( ) NAMED_UNIT ( * ) SI_UNIT ( .MILLI., .METRE. ) );
#20743=B_SPLINE_CURVE_WITH_KNOTS ( 'NONE', 3,
 ( #22989, #17446, #53, #18154 ),
 .UNSPECIFIED., .F., .F.,
 ( 4, 4 ),
 ( 2.309401076744506391E-07, 0.004330357959029864159 ),
 .UNSPECIFIED. ) ;
#20784=CARTESIAN_POINT ( 'NONE',  ( 0.000000000000000000, 0.000000000000000000, 0.000000000000000000 ) ) ;
#20809=EDGE_LOOP ( 'NONE', ( #10398, #9569, #13330 ) ) ;
#20820=COLOUR_RGB ( '', 0.40784314, 0.44705882, 0.49803922) ;
#20821=EDGE_CURVE ( 'NONE', #20563, #16003, #11310, .T. ) ;
#20839=EDGE_LOOP ( 'NONE', ( #19216, #8788, #9912 ) ) ;
#20858=PRODUCT_DEFINITION ( 'UNKNOWN', '', #16133, #9125 ) ;
#20897=VECTOR ( 'NONE', #13403, 1000.000000000000000 ) ;
#20900=CARTESIAN_POINT ( 'NONE',  ( -6.938893903907228378E-14, 4.999999999999976907, -4.163336342344337027E-14 ) ) ;
#20966=ORIENTED_EDGE ( 'NONE', *, *, #16750, .F. ) ;
#21000=ORIENTED_EDGE ( 'NONE', *, *, #15119, .T. ) ;
#21100=CARTESIAN_POINT ( 'NONE',  ( 4.330127018922088844, -1.387778780781445676E-13, 7.500000000000027534 ) ) ;
#21120=CONICAL_SURFACE ( 'NONE', #10954, 7.500000000000001776, 1.308996938995750092 ) ;
#21129=FACE_OUTER_BOUND ( 'NONE', #20809, .T. ) ;
#21133=VECTOR ( 'NONE', #17440, 1000.000000000000000 ) ;
#21180=ORIENTED_EDGE ( 'NONE', *, *, #4901, .F. ) ;
#21250=EDGE_CURVE ( 'NONE', #23120, #5408, #6462, .T. ) ;
#21320=EDGE_CURVE ( 'NONE', #7483, #17574, #16845, .T. ) ;
#21350=PRODUCT ( 'Lock nut', 'Lock nut', '', ( #3206 ) ) ;
#21363=ORIENTED_EDGE ( 'NONE', *, *, #9941, .T. ) ;
#21539=CARTESIAN_POINT ( 'NONE',  ( 5.051814855409154426, 4.882486540518890195, -6.250000000000007105 ) ) ;
#21585=ORIENTED_EDGE ( 'NONE', *, *, #18133, .T. ) ;
#21616=ADVANCED_FACE ( 'NONE', ( #4772 ), #11943, .F. ) ;
#21652=VECTOR ( 'NONE', #10261, 1000.000000000000000 ) ;
#21695=ORIENTED_EDGE ( 'NONE', *, *, #20327, .T. ) ;
#21697=VERTEX_POINT ( 'NONE', #5004 ) ;
#21728=EDGE_LOOP ( 'NONE', ( #3384, #22034, #22178 ) ) ;
#21730=DIRECTION ( 'NONE',  ( -5.551115123561405253E-17, -1.000000000000000000, -2.256980353643891447E-27 ) ) ;
#21750=DIRECTION ( 'NONE',  ( 5.551115123561405253E-17, 1.000000000000000000, 2.256980353643891447E-27 ) ) ;
#21777=DIRECTION ( 'NONE',  ( -0.8660254037844387076, 2.506296930348934952E-16, 0.4999999999999999445 ) ) ;
#21786=ORIENTED_EDGE ( 'NONE', *, *, #1487, .F. ) ;
#21800=DIRECTION ( 'NONE',  ( -9.693457064947022734E-26, 0.000000000000000000, 1.000000000000000000 ) ) ;
#21806=PLANE ( 'NONE',  #6281 ) ;
#21823=CARTESIAN_POINT ( 'NONE',  ( 0.000000000000000000, 0.000000000000000000, 0.000000000000000000 ) ) ;
#21842=FACE_OUTER_BOUND ( 'NONE', #339, .T. ) ;
#21854=LINE ( 'NONE', #5748, #14227 ) ;
#21873=CARTESIAN_POINT ( 'NONE',  ( 8.660254037844413944, 4.689110867544616035, 2.775557561562891351E-14 ) ) ;
#21887=VECTOR ( 'NONE', #20202, 1000.000000000000000 ) ;
#21910=DIRECTION ( 'NONE',  ( -9.693457064947022734E-26, 0.000000000000000000, 1.000000000000000000 ) ) ;
#21923=ORIENTED_EDGE ( 'NONE', *, *, #16750, .T. ) ;
#21971=EDGE_CURVE ( 'NONE', #5408, #14506, #3453, .T. ) ;
#21986=DIRECTION ( 'NONE',  ( 5.551115123561405253E-17, 1.000000000000000000, -5.963788443470795439E-28 ) ) ;
#22034=ORIENTED_EDGE ( 'NONE', *, *, #18696, .T. ) ;
#22107=ADVANCED_FACE ( 'NONE', ( #19803 ), #21806, .F. ) ;
#22110=CARTESIAN_POINT ( 'NONE',  ( 0.000000000000000000, 0.000000000000000000, 0.000000000000000000 ) ) ;
#22115=AXIS2_PLACEMENT_3D ( 'NONE', #4943, #2963, #5306 ) ;
#22136=CARTESIAN_POINT ( 'NONE',  ( 4.330127018922103055, 4.999999999999838352, 7.499999999999971578 ) ) ;
#22164=( GEOMETRIC_REPRESENTATION_CONTEXT ( 3 ) GLOBAL_UNCERTAINTY_ASSIGNED_CONTEXT ( ( #5844 ) ) GLOBAL_UNIT_ASSIGNED_CONTEXT ( ( #18615, #18727, #741 ) ) REPRESENTATION_CONTEXT ( 'NONE', 'WORKASPACE' ) );
#22165=DIRECTION ( 'NONE',  ( -5.551115123561405253E-17, -1.000000000000000000, -2.256980353643891447E-27 ) ) ;
#22178=ORIENTED_EDGE ( 'NONE', *, *, #8083, .F. ) ;
#22313=CARTESIAN_POINT ( 'NONE',  ( -7.938566201357348362, 4.882486540518906182, -1.249999999999981126 ) ) ;
#22321=DIRECTION ( 'NONE',  ( 0.4999999999999998890, 2.286725509617064044E-17, -0.8660254037844387076 ) ) ;
#22334=CARTESIAN_POINT ( 'NONE',  ( -6.495190528383328221, 1.387778780781445676E-14, -3.749999999999989342 ) ) ;
#22360=AXIS2_PLACEMENT_3D ( 'NONE', #6229, #11861, #1055 ) ;
#22374=CARTESIAN_POINT ( 'NONE',  ( 4.330127018922110160, 4.999999999999976907, -7.500000000000003553 ) ) ;
#22406=VECTOR ( 'NONE', #7163, 1000.000000000000000 ) ;
#22436=ORIENTED_EDGE ( 'NONE', *, *, #16231, .F. ) ;
#22450=EDGE_CURVE ( 'NONE', #14506, #1035, #16657, .T. ) ;
#22499=( NAMED_UNIT ( * ) PLANE_ANGLE_UNIT ( ) SI_UNIT ( $, .RADIAN. ) );
#22584=ORIENTED_EDGE ( 'NONE', *, *, #16585, .F. ) ;
#22701=DIRECTION ( 'NONE',  ( -9.693647360340828445E-26, 0.000000000000000000, 1.000000000000000000 ) ) ;
#22744=CONICAL_SURFACE ( 'NONE', #12590, 7.499999999999998224, 1.308996938995750092 ) ;
#22784=CARTESIAN_POINT ( 'NONE',  ( -4.330127018922179438, 4.999999999999976907, -7.500000000000000000 ) ) ;
#22809=CARTESIAN_POINT ( 'NONE',  ( 0.000000000000000000, 0.000000000000000000, 0.000000000000000000 ) ) ;
#22858=CARTESIAN_POINT ( 'NONE',  ( -4.330127018922234505, -2.775557561562891351E-14, -7.499999999999989342 ) ) ;
#22867=LINE ( 'NONE', #21100, #21133 ) ;
#22954=CARTESIAN_POINT ( 'NONE',  ( -4.330127018922248716, 4.689110867544532546, 7.500000000000007105 ) ) ;
#22962=EDGE_CURVE ( 'NONE', #17095, #9471, #20743, .T. ) ;
#22989=CARTESIAN_POINT ( 'NONE',  ( 4.330127018922110160, 4.689110867544560080, 7.499999999999985789 ) ) ;
#23103=EDGE_CURVE ( 'NONE', #21697, #12036, #14562, .T. ) ;
#23120=VERTEX_POINT ( 'NONE', #2606 ) ;
#23199=FACE_OUTER_BOUND ( 'NONE', #954, .T. ) ;
#23204=SHAPE_DEFINITION_REPRESENTATION ( #6671, #17992 ) ;
ENDSEC;
END-ISO-10303-21;
